ISO-10303-21;
HEADER;
/* Generated by software containing ST-Developer
 * from STEP Tools, Inc. (www.steptools.com) 
 */

FILE_DESCRIPTION(
/* description */ ('Crank-driven oscillating fan base (mechanism only)'),

/* implementation_level */ '2;1');

FILE_NAME(
/* name */ 'Cap Screw - M4x16.step',
/* time_stamp */ '2026-10-28T03:25:00-07:00',
/* author */ (''),
/* organization */ (''),
/* preprocessor_version */ 'ST-DEVELOPER v20.2',
/* originating_system */ 'Autodesk Translation Framework v15.17.0.0',
/* authorisation */ '');

FILE_SCHEMA (('AUTOMOTIVE_DESIGN { 1 0 10303 214 3 1 1 }'));
ENDSEC;

DATA;
#10=MECHANICAL_DESIGN_GEOMETRIC_PRESENTATION_REPRESENTATION('',(#480),#11916);
#303=CONICAL_SURFACE('',#7267,0.325,0.785398163397448);
#304=CONICAL_SURFACE('',#7271,0.335,0.785398163397448);
#305=CONICAL_SURFACE('',#7275,0.21,0.463647609000806);
#306=CONICAL_SURFACE('',#7279,0.18,0.785398163397448);
#311=ORIENTED_CLOSED_SHELL('',*,#6112,.F.);
#314=BREP_WITH_VOIDS('Body1',#6111,(#311));
#392=SHAPE_REPRESENTATION_RELATIONSHIP('SRR','None',#12119,#432);
#432=ADVANCED_BREP_SHAPE_REPRESENTATION('',(#314),#11910);
#480=STYLED_ITEM('',(#12382),#314);
#682=FACE_BOUND('',#1744,.T.);
#856=PLANE('',#7265);
#857=PLANE('',#7273);
#858=PLANE('',#7281);
#859=PLANE('',#7282);
#860=PLANE('',#7283);
#861=PLANE('',#7284);
#862=PLANE('',#7285);
#863=PLANE('',#7286);
#864=PLANE('',#7287);
#865=PLANE('',#7288);
#866=PLANE('',#7289);
#1212=FACE_OUTER_BOUND('',#1739,.T.);
#1213=FACE_OUTER_BOUND('',#1740,.T.);
#1214=FACE_OUTER_BOUND('',#1741,.T.);
#1215=FACE_OUTER_BOUND('',#1742,.T.);
#1216=FACE_OUTER_BOUND('',#1743,.T.);
#1217=FACE_OUTER_BOUND('',#1745,.T.);
#1218=FACE_OUTER_BOUND('',#1746,.T.);
#1219=FACE_OUTER_BOUND('',#1747,.T.);
#1220=FACE_OUTER_BOUND('',#1748,.T.);
#1221=FACE_OUTER_BOUND('',#1749,.T.);
#1222=FACE_OUTER_BOUND('',#1750,.T.);
#1223=FACE_OUTER_BOUND('',#1751,.T.);
#1224=FACE_OUTER_BOUND('',#1752,.T.);
#1225=FACE_OUTER_BOUND('',#1753,.T.);
#1226=FACE_OUTER_BOUND('',#1754,.T.);
#1227=FACE_OUTER_BOUND('',#1755,.T.);
#1228=FACE_OUTER_BOUND('',#1756,.T.);
#1739=EDGE_LOOP('',(#5362));
#1740=EDGE_LOOP('',(#5363,#5364,#5365,#5366));
#1741=EDGE_LOOP('',(#5367,#5368,#5369,#5370));
#1742=EDGE_LOOP('',(#5371,#5372,#5373,#5374));
#1743=EDGE_LOOP('',(#5375));
#1744=EDGE_LOOP('',(#5376));
#1745=EDGE_LOOP('',(#5377,#5378,#5379,#5380));
#1746=EDGE_LOOP('',(#5381,#5382,#5383,#5384));
#1747=EDGE_LOOP('',(#5385,#5386,#5387,#5388));
#1748=EDGE_LOOP('',(#5389));
#1749=EDGE_LOOP('',(#5390,#5391,#5392,#5393));
#1750=EDGE_LOOP('',(#5394,#5395,#5396,#5397));
#1751=EDGE_LOOP('',(#5398,#5399,#5400,#5401));
#1752=EDGE_LOOP('',(#5402,#5403,#5404,#5405));
#1753=EDGE_LOOP('',(#5406,#5407,#5408,#5409));
#1754=EDGE_LOOP('',(#5410,#5411,#5412,#5413));
#1755=EDGE_LOOP('',(#5414,#5415,#5416,#5417,#5418,#5419));
#1756=EDGE_LOOP('',(#5420,#5421,#5422,#5423,#5424,#5425));
#2070=LINE('',#11563,#2403);
#2071=LINE('',#11567,#2404);
#2072=LINE('',#11571,#2405);
#2073=LINE('',#11578,#2406);
#2074=LINE('',#11582,#2407);
#2075=LINE('',#11586,#2408);
#2076=LINE('',#11591,#2409);
#2077=LINE('',#11593,#2410);
#2078=LINE('',#11595,#2411);
#2079=LINE('',#11596,#2412);
#2080=LINE('',#11599,#2413);
#2081=LINE('',#11601,#2414);
#2082=LINE('',#11602,#2415);
#2083=LINE('',#11605,#2416);
#2084=LINE('',#11607,#2417);
#2085=LINE('',#11608,#2418);
#2086=LINE('',#11611,#2419);
#2087=LINE('',#11613,#2420);
#2088=LINE('',#11614,#2421);
#2089=LINE('',#11617,#2422);
#2090=LINE('',#11619,#2423);
#2091=LINE('',#11620,#2424);
#2092=LINE('',#11622,#2425);
#2093=LINE('',#11623,#2426);
#2403=VECTOR('',#9103,0.325);
#2404=VECTOR('',#9108,0.35);
#2405=VECTOR('',#9113,0.335);
#2406=VECTOR('',#9122,0.21);
#2407=VECTOR('',#9127,0.2);
#2408=VECTOR('',#9132,0.18);
#2409=VECTOR('',#9137,1.);
#2410=VECTOR('',#9138,1.);
#2411=VECTOR('',#9139,1.);
#2412=VECTOR('',#9140,1.);
#2413=VECTOR('',#9143,1.);
#2414=VECTOR('',#9144,1.);
#2415=VECTOR('',#9145,1.);
#2416=VECTOR('',#9148,1.);
#2417=VECTOR('',#9149,1.);
#2418=VECTOR('',#9150,1.);
#2419=VECTOR('',#9153,1.);
#2420=VECTOR('',#9154,1.);
#2421=VECTOR('',#9155,1.);
#2422=VECTOR('',#9158,1.);
#2423=VECTOR('',#9159,1.);
#2424=VECTOR('',#9160,1.);
#2425=VECTOR('',#9163,1.);
#2426=VECTOR('',#9164,1.);
#2798=CIRCLE('',#7266,0.3);
#2799=CIRCLE('',#7268,0.35);
#2800=CIRCLE('',#7270,0.35);
#2801=CIRCLE('',#7272,0.32);
#2802=CIRCLE('',#7274,0.22);
#2803=CIRCLE('',#7276,0.1954);
#2804=CIRCLE('',#7278,0.1954);
#2805=CIRCLE('',#7280,0.16);
#3270=VERTEX_POINT('',#11558);
#3271=VERTEX_POINT('',#11561);
#3272=VERTEX_POINT('',#11565);
#3273=VERTEX_POINT('',#11569);
#3274=VERTEX_POINT('',#11573);
#3275=VERTEX_POINT('',#11576);
#3276=VERTEX_POINT('',#11580);
#3277=VERTEX_POINT('',#11584);
#3278=VERTEX_POINT('',#11589);
#3279=VERTEX_POINT('',#11590);
#3280=VERTEX_POINT('',#11592);
#3281=VERTEX_POINT('',#11594);
#3282=VERTEX_POINT('',#11598);
#3283=VERTEX_POINT('',#11600);
#3284=VERTEX_POINT('',#11604);
#3285=VERTEX_POINT('',#11606);
#3286=VERTEX_POINT('',#11610);
#3287=VERTEX_POINT('',#11612);
#3288=VERTEX_POINT('',#11616);
#3289=VERTEX_POINT('',#11618);
#3976=EDGE_CURVE('',#3270,#3270,#2798,.T.);
#3977=EDGE_CURVE('',#3271,#3271,#2799,.T.);
#3978=EDGE_CURVE('',#3271,#3270,#2070,.T.);
#3979=EDGE_CURVE('',#3272,#3272,#2800,.T.);
#3980=EDGE_CURVE('',#3272,#3271,#2071,.T.);
#3981=EDGE_CURVE('',#3273,#3273,#2801,.T.);
#3982=EDGE_CURVE('',#3273,#3272,#2072,.T.);
#3983=EDGE_CURVE('',#3274,#3274,#2802,.T.);
#3984=EDGE_CURVE('',#3275,#3275,#2803,.F.);
#3985=EDGE_CURVE('',#3275,#3274,#2073,.T.);
#3986=EDGE_CURVE('',#3276,#3276,#2804,.F.);
#3987=EDGE_CURVE('',#3276,#3275,#2074,.T.);
#3988=EDGE_CURVE('',#3277,#3277,#2805,.T.);
#3989=EDGE_CURVE('',#3277,#3276,#2075,.T.);
#3990=EDGE_CURVE('',#3278,#3279,#2076,.T.);
#3991=EDGE_CURVE('',#3279,#3280,#2077,.T.);
#3992=EDGE_CURVE('',#3280,#3281,#2078,.T.);
#3993=EDGE_CURVE('',#3278,#3281,#2079,.T.);
#3994=EDGE_CURVE('',#3279,#3282,#2080,.T.);
#3995=EDGE_CURVE('',#3282,#3283,#2081,.T.);
#3996=EDGE_CURVE('',#3283,#3280,#2082,.T.);
#3997=EDGE_CURVE('',#3282,#3284,#2083,.T.);
#3998=EDGE_CURVE('',#3284,#3285,#2084,.T.);
#3999=EDGE_CURVE('',#3285,#3283,#2085,.T.);
#4000=EDGE_CURVE('',#3284,#3286,#2086,.T.);
#4001=EDGE_CURVE('',#3286,#3287,#2087,.T.);
#4002=EDGE_CURVE('',#3287,#3285,#2088,.T.);
#4003=EDGE_CURVE('',#3286,#3288,#2089,.T.);
#4004=EDGE_CURVE('',#3288,#3289,#2090,.T.);
#4005=EDGE_CURVE('',#3289,#3287,#2091,.T.);
#4006=EDGE_CURVE('',#3288,#3278,#2092,.T.);
#4007=EDGE_CURVE('',#3281,#3289,#2093,.T.);
#5362=ORIENTED_EDGE('',*,*,#3976,.F.);
#5363=ORIENTED_EDGE('',*,*,#3977,.F.);
#5364=ORIENTED_EDGE('',*,*,#3978,.T.);
#5365=ORIENTED_EDGE('',*,*,#3976,.T.);
#5366=ORIENTED_EDGE('',*,*,#3978,.F.);
#5367=ORIENTED_EDGE('',*,*,#3979,.F.);
#5368=ORIENTED_EDGE('',*,*,#3980,.T.);
#5369=ORIENTED_EDGE('',*,*,#3977,.T.);
#5370=ORIENTED_EDGE('',*,*,#3980,.F.);
#5371=ORIENTED_EDGE('',*,*,#3981,.F.);
#5372=ORIENTED_EDGE('',*,*,#3982,.T.);
#5373=ORIENTED_EDGE('',*,*,#3979,.T.);
#5374=ORIENTED_EDGE('',*,*,#3982,.F.);
#5375=ORIENTED_EDGE('',*,*,#3981,.T.);
#5376=ORIENTED_EDGE('',*,*,#3983,.F.);
#5377=ORIENTED_EDGE('',*,*,#3984,.F.);
#5378=ORIENTED_EDGE('',*,*,#3985,.T.);
#5379=ORIENTED_EDGE('',*,*,#3983,.T.);
#5380=ORIENTED_EDGE('',*,*,#3985,.F.);
#5381=ORIENTED_EDGE('',*,*,#3986,.F.);
#5382=ORIENTED_EDGE('',*,*,#3987,.T.);
#5383=ORIENTED_EDGE('',*,*,#3984,.T.);
#5384=ORIENTED_EDGE('',*,*,#3987,.F.);
#5385=ORIENTED_EDGE('',*,*,#3988,.F.);
#5386=ORIENTED_EDGE('',*,*,#3989,.T.);
#5387=ORIENTED_EDGE('',*,*,#3986,.T.);
#5388=ORIENTED_EDGE('',*,*,#3989,.F.);
#5389=ORIENTED_EDGE('',*,*,#3988,.T.);
#5390=ORIENTED_EDGE('',*,*,#3990,.T.);
#5391=ORIENTED_EDGE('',*,*,#3991,.T.);
#5392=ORIENTED_EDGE('',*,*,#3992,.T.);
#5393=ORIENTED_EDGE('',*,*,#3993,.F.);
#5394=ORIENTED_EDGE('',*,*,#3994,.T.);
#5395=ORIENTED_EDGE('',*,*,#3995,.T.);
#5396=ORIENTED_EDGE('',*,*,#3996,.T.);
#5397=ORIENTED_EDGE('',*,*,#3991,.F.);
#5398=ORIENTED_EDGE('',*,*,#3997,.T.);
#5399=ORIENTED_EDGE('',*,*,#3998,.T.);
#5400=ORIENTED_EDGE('',*,*,#3999,.T.);
#5401=ORIENTED_EDGE('',*,*,#3995,.F.);
#5402=ORIENTED_EDGE('',*,*,#4000,.T.);
#5403=ORIENTED_EDGE('',*,*,#4001,.T.);
#5404=ORIENTED_EDGE('',*,*,#4002,.T.);
#5405=ORIENTED_EDGE('',*,*,#3998,.F.);
#5406=ORIENTED_EDGE('',*,*,#4003,.T.);
#5407=ORIENTED_EDGE('',*,*,#4004,.T.);
#5408=ORIENTED_EDGE('',*,*,#4005,.T.);
#5409=ORIENTED_EDGE('',*,*,#4001,.F.);
#5410=ORIENTED_EDGE('',*,*,#4006,.T.);
#5411=ORIENTED_EDGE('',*,*,#3993,.T.);
#5412=ORIENTED_EDGE('',*,*,#4007,.T.);
#5413=ORIENTED_EDGE('',*,*,#4004,.F.);
#5414=ORIENTED_EDGE('',*,*,#4006,.F.);
#5415=ORIENTED_EDGE('',*,*,#4003,.F.);
#5416=ORIENTED_EDGE('',*,*,#4000,.F.);
#5417=ORIENTED_EDGE('',*,*,#3997,.F.);
#5418=ORIENTED_EDGE('',*,*,#3994,.F.);
#5419=ORIENTED_EDGE('',*,*,#3990,.F.);
#5420=ORIENTED_EDGE('',*,*,#4007,.F.);
#5421=ORIENTED_EDGE('',*,*,#3992,.F.);
#5422=ORIENTED_EDGE('',*,*,#3996,.F.);
#5423=ORIENTED_EDGE('',*,*,#3999,.F.);
#5424=ORIENTED_EDGE('',*,*,#4002,.F.);
#5425=ORIENTED_EDGE('',*,*,#4005,.F.);
#5680=CYLINDRICAL_SURFACE('',#7269,0.35);
#5681=CYLINDRICAL_SURFACE('',#7277,0.1954);
#6018=ADVANCED_FACE('',(#1212),#856,.T.);
#6019=ADVANCED_FACE('',(#1213),#303,.T.);
#6020=ADVANCED_FACE('',(#1214),#5680,.T.);
#6021=ADVANCED_FACE('',(#1215),#304,.T.);
#6022=ADVANCED_FACE('',(#1216,#682),#857,.T.);
#6023=ADVANCED_FACE('',(#1217),#305,.T.);
#6024=ADVANCED_FACE('',(#1218),#5681,.T.);
#6025=ADVANCED_FACE('',(#1219),#306,.T.);
#6026=ADVANCED_FACE('',(#1220),#858,.T.);
#6027=ADVANCED_FACE('',(#1221),#859,.F.);
#6028=ADVANCED_FACE('',(#1222),#860,.F.);
#6029=ADVANCED_FACE('',(#1223),#861,.F.);
#6030=ADVANCED_FACE('',(#1224),#862,.F.);
#6031=ADVANCED_FACE('',(#1225),#863,.F.);
#6032=ADVANCED_FACE('',(#1226),#864,.F.);
#6033=ADVANCED_FACE('',(#1227),#865,.F.);
#6034=ADVANCED_FACE('',(#1228),#866,.F.);
#6111=CLOSED_SHELL('',(#6018,#6019,#6020,#6021,#6022,#6023,#6024,#6025,
#6026));
#6112=CLOSED_SHELL('',(#6027,#6028,#6029,#6030,#6031,#6032,#6033,#6034));
#7264=AXIS2_PLACEMENT_3D('',#11556,#9093,#9094);
#7265=AXIS2_PLACEMENT_3D('',#11557,#9095,#9096);
#7266=AXIS2_PLACEMENT_3D('',#11559,#9097,#9098);
#7267=AXIS2_PLACEMENT_3D('',#11560,#9099,#9100);
#7268=AXIS2_PLACEMENT_3D('',#11562,#9101,#9102);
#7269=AXIS2_PLACEMENT_3D('',#11564,#9104,#9105);
#7270=AXIS2_PLACEMENT_3D('',#11566,#9106,#9107);
#7271=AXIS2_PLACEMENT_3D('',#11568,#9109,#9110);
#7272=AXIS2_PLACEMENT_3D('',#11570,#9111,#9112);
#7273=AXIS2_PLACEMENT_3D('',#11572,#9114,#9115);
#7274=AXIS2_PLACEMENT_3D('',#11574,#9116,#9117);
#7275=AXIS2_PLACEMENT_3D('',#11575,#9118,#9119);
#7276=AXIS2_PLACEMENT_3D('',#11577,#9120,#9121);
#7277=AXIS2_PLACEMENT_3D('',#11579,#9123,#9124);
#7278=AXIS2_PLACEMENT_3D('',#11581,#9125,#9126);
#7279=AXIS2_PLACEMENT_3D('',#11583,#9128,#9129);
#7280=AXIS2_PLACEMENT_3D('',#11585,#9130,#9131);
#7281=AXIS2_PLACEMENT_3D('',#11587,#9133,#9134);
#7282=AXIS2_PLACEMENT_3D('',#11588,#9135,#9136);
#7283=AXIS2_PLACEMENT_3D('',#11597,#9141,#9142);
#7284=AXIS2_PLACEMENT_3D('',#11603,#9146,#9147);
#7285=AXIS2_PLACEMENT_3D('',#11609,#9151,#9152);
#7286=AXIS2_PLACEMENT_3D('',#11615,#9156,#9157);
#7287=AXIS2_PLACEMENT_3D('',#11621,#9161,#9162);
#7288=AXIS2_PLACEMENT_3D('',#11624,#9165,#9166);
#7289=AXIS2_PLACEMENT_3D('',#11625,#9167,#9168);
#9093=DIRECTION('axis',(0.,0.,1.));
#9094=DIRECTION('refdir',(1.,0.,0.));
#9095=DIRECTION('center_axis',(0.,1.,0.));
#9096=DIRECTION('ref_axis',(0.,0.,1.));
#9097=DIRECTION('center_axis',(0.,-1.,0.));
#9098=DIRECTION('ref_axis',(1.,0.,0.));
#9099=DIRECTION('center_axis',(0.,-1.,0.));
#9100=DIRECTION('ref_axis',(1.,0.,0.));
#9101=DIRECTION('center_axis',(0.,-1.,0.));
#9102=DIRECTION('ref_axis',(1.,0.,0.));
#9103=DIRECTION('',(0.707106781186547,0.707106781186548,8.65956056235493E-17));
#9104=DIRECTION('center_axis',(0.,-1.,0.));
#9105=DIRECTION('ref_axis',(1.,0.,0.));
#9106=DIRECTION('center_axis',(0.,-1.,0.));
#9107=DIRECTION('ref_axis',(1.,0.,0.));
#9108=DIRECTION('',(0.,1.,0.));
#9109=DIRECTION('center_axis',(0.,1.,0.));
#9110=DIRECTION('ref_axis',(1.,0.,0.));
#9111=DIRECTION('center_axis',(0.,-1.,0.));
#9112=DIRECTION('ref_axis',(1.,0.,0.));
#9113=DIRECTION('',(-0.707106781186547,0.707106781186548,-8.65956056235493E-17));
#9114=DIRECTION('center_axis',(0.,-1.,0.));
#9115=DIRECTION('ref_axis',(0.,0.,-1.));
#9116=DIRECTION('center_axis',(0.,-1.,0.));
#9117=DIRECTION('ref_axis',(1.,0.,0.));
#9118=DIRECTION('center_axis',(0.,1.,0.));
#9119=DIRECTION('ref_axis',(1.,0.,0.));
#9120=DIRECTION('center_axis',(0.,1.,0.));
#9121=DIRECTION('ref_axis',(1.,0.,0.));
#9122=DIRECTION('',(-0.447213595499958,0.894427190999916,-5.47678698264203E-17));
#9123=DIRECTION('center_axis',(0.,-1.,0.));
#9124=DIRECTION('ref_axis',(1.,0.,0.));
#9125=DIRECTION('center_axis',(0.,1.,0.));
#9126=DIRECTION('ref_axis',(1.,0.,0.));
#9127=DIRECTION('',(0.,1.,0.));
#9128=DIRECTION('center_axis',(0.,1.,0.));
#9129=DIRECTION('ref_axis',(1.,0.,0.));
#9130=DIRECTION('center_axis',(0.,-1.,0.));
#9131=DIRECTION('ref_axis',(1.,0.,0.));
#9132=DIRECTION('',(-0.707106781186547,0.707106781186548,-8.65956056235493E-17));
#9133=DIRECTION('center_axis',(0.,-1.,0.));
#9134=DIRECTION('ref_axis',(0.,0.,-1.));
#9135=DIRECTION('center_axis',(0.866025403784439,0.,-0.5));
#9136=DIRECTION('ref_axis',(0.5,0.,0.866025403784439));
#9137=DIRECTION('',(-0.5,0.,-0.866025403784439));
#9138=DIRECTION('',(0.,-1.,0.));
#9139=DIRECTION('',(0.5,0.,0.866025403784439));
#9140=DIRECTION('',(0.,-1.,0.));
#9141=DIRECTION('center_axis',(1.60246890531964E-16,0.,-1.));
#9142=DIRECTION('ref_axis',(1.,0.,1.60246890531964E-16));
#9143=DIRECTION('',(-1.,0.,-1.60246890531964E-16));
#9144=DIRECTION('',(0.,-1.,0.));
#9145=DIRECTION('',(1.,0.,1.60246890531964E-16));
#9146=DIRECTION('center_axis',(-0.866025403784439,0.,-0.5));
#9147=DIRECTION('ref_axis',(0.5,0.,-0.866025403784439));
#9148=DIRECTION('',(-0.5,0.,0.866025403784439));
#9149=DIRECTION('',(0.,-1.,0.));
#9150=DIRECTION('',(0.5,0.,-0.866025403784439));
#9151=DIRECTION('center_axis',(-0.866025403784439,0.,0.5));
#9152=DIRECTION('ref_axis',(-0.5,0.,-0.866025403784439));
#9153=DIRECTION('',(0.5,0.,0.866025403784439));
#9154=DIRECTION('',(0.,-1.,0.));
#9155=DIRECTION('',(-0.5,0.,-0.866025403784439));
#9156=DIRECTION('center_axis',(-1.60246890531964E-16,0.,1.));
#9157=DIRECTION('ref_axis',(-1.,0.,-1.60246890531964E-16));
#9158=DIRECTION('',(1.,0.,1.60246890531964E-16));
#9159=DIRECTION('',(0.,-1.,0.));
#9160=DIRECTION('',(-1.,0.,-1.60246890531964E-16));
#9161=DIRECTION('center_axis',(0.866025403784439,0.,0.5));
#9162=DIRECTION('ref_axis',(-0.5,0.,0.866025403784439));
#9163=DIRECTION('',(0.5,0.,-0.866025403784439));
#9164=DIRECTION('',(-0.5,0.,0.866025403784439));
#9165=DIRECTION('center_axis',(0.,1.,0.));
#9166=DIRECTION('ref_axis',(1.,0.,0.));
#9167=DIRECTION('center_axis',(0.,-1.,0.));
#9168=DIRECTION('ref_axis',(0.,0.,-1.));
#11556=CARTESIAN_POINT('',(0.,0.,0.));
#11557=CARTESIAN_POINT('Origin',(0.3,0.4,0.));
#11558=CARTESIAN_POINT('',(-0.3,0.4,-3.67394039744206E-17));
#11559=CARTESIAN_POINT('Origin',(0.,0.4,0.));
#11560=CARTESIAN_POINT('Origin',(0.,0.375,0.));
#11561=CARTESIAN_POINT('',(-0.35,0.35,-4.28626379701573E-17));
#11562=CARTESIAN_POINT('Origin',(0.,0.35,0.));
#11563=CARTESIAN_POINT('',(-0.325,0.375,-3.9801020972289E-17));
#11564=CARTESIAN_POINT('Origin',(0.,0.19,0.));
#11565=CARTESIAN_POINT('',(-0.35,0.03,-4.28626379701574E-17));
#11566=CARTESIAN_POINT('Origin',(0.,0.03,0.));
#11567=CARTESIAN_POINT('',(-0.35,0.19,-4.28626379701574E-17));
#11568=CARTESIAN_POINT('Origin',(0.,0.0149999999999999,0.));
#11569=CARTESIAN_POINT('',(-0.32,-3.29597460435593E-17,-3.91886975727153E-17));
#11570=CARTESIAN_POINT('Origin',(0.,0.,0.));
#11571=CARTESIAN_POINT('',(-0.335,0.0149999999999999,-4.10256677714363E-17));
#11572=CARTESIAN_POINT('Origin',(0.22,0.,0.));
#11573=CARTESIAN_POINT('',(-0.22,-6.93889390390723E-18,-2.69422295812418E-17));
#11574=CARTESIAN_POINT('Origin',(0.,0.,0.));
#11575=CARTESIAN_POINT('Origin',(0.,-0.02,0.));
#11576=CARTESIAN_POINT('',(-0.1954,-0.0492,2.39295984553393E-17));
#11577=CARTESIAN_POINT('Origin',(0.,-0.0492,0.));
#11578=CARTESIAN_POINT('',(-0.21,-0.02,-2.57175827820944E-17));
#11579=CARTESIAN_POINT('Origin',(0.,-0.8,0.));
#11580=CARTESIAN_POINT('',(-0.1954,-1.5646,2.39295984553393E-17));
#11581=CARTESIAN_POINT('Origin',(0.,-1.5646,0.));
#11582=CARTESIAN_POINT('',(-0.1954,-0.8,-2.39295984553393E-17));
#11583=CARTESIAN_POINT('Origin',(0.,-1.58,0.));
#11584=CARTESIAN_POINT('',(-0.16,-1.6,-1.95943487863577E-17));
#11585=CARTESIAN_POINT('Origin',(0.,-1.6,0.));
#11586=CARTESIAN_POINT('',(-0.18,-1.58,-2.20436423846524E-17));
#11587=CARTESIAN_POINT('Origin',(0.,-1.6,0.));
#11588=CARTESIAN_POINT('Origin',(0.0866025403784439,-0.4,-0.15));
#11589=CARTESIAN_POINT('',(0.173205080756888,-0.4,0.));
#11590=CARTESIAN_POINT('',(0.0866025403784439,-0.4,-0.15));
#11591=CARTESIAN_POINT('',(0.173205080756888,-0.4,0.));
#11592=CARTESIAN_POINT('',(0.0866025403784439,-0.64,-0.15));
#11593=CARTESIAN_POINT('',(0.0866025403784439,-0.4,-0.15));
#11594=CARTESIAN_POINT('',(0.173205080756888,-0.64,0.));
#11595=CARTESIAN_POINT('',(0.173205080756888,-0.64,0.));
#11596=CARTESIAN_POINT('',(0.173205080756888,-0.4,0.));
#11597=CARTESIAN_POINT('Origin',(-0.0866025403784438,-0.4,-0.15));
#11598=CARTESIAN_POINT('',(-0.0866025403784438,-0.4,-0.15));
#11599=CARTESIAN_POINT('',(0.0866025403784439,-0.4,-0.15));
#11600=CARTESIAN_POINT('',(-0.0866025403784438,-0.64,-0.15));
#11601=CARTESIAN_POINT('',(-0.0866025403784438,-0.4,-0.15));
#11602=CARTESIAN_POINT('',(0.0866025403784439,-0.64,-0.15));
#11603=CARTESIAN_POINT('Origin',(-0.173205080756888,-0.4,-2.77555756156289E-17));
#11604=CARTESIAN_POINT('',(-0.173205080756888,-0.4,-2.12115047744981E-17));
#11605=CARTESIAN_POINT('',(-0.0866025403784438,-0.4,-0.15));
#11606=CARTESIAN_POINT('',(-0.173205080756888,-0.64,-2.77555756156289E-17));
#11607=CARTESIAN_POINT('',(-0.173205080756888,-0.4,-2.12115047744981E-17));
#11608=CARTESIAN_POINT('',(-0.0866025403784438,-0.64,-0.15));
#11609=CARTESIAN_POINT('Origin',(-0.0866025403784439,-0.4,0.15));
#11610=CARTESIAN_POINT('',(-0.0866025403784439,-0.4,0.15));
#11611=CARTESIAN_POINT('',(-0.173205080756888,-0.4,-2.12115047744981E-17));
#11612=CARTESIAN_POINT('',(-0.0866025403784439,-0.64,0.15));
#11613=CARTESIAN_POINT('',(-0.0866025403784439,-0.4,0.15));
#11614=CARTESIAN_POINT('',(-0.173205080756888,-0.64,-2.12115047744981E-17));
#11615=CARTESIAN_POINT('Origin',(0.0866025403784439,-0.4,0.15));
#11616=CARTESIAN_POINT('',(0.0866025403784439,-0.4,0.15));
#11617=CARTESIAN_POINT('',(-0.0866025403784439,-0.4,0.15));
#11618=CARTESIAN_POINT('',(0.0866025403784439,-0.64,0.15));
#11619=CARTESIAN_POINT('',(0.0866025403784439,-0.4,0.15));
#11620=CARTESIAN_POINT('',(-0.0866025403784439,-0.64,0.15));
#11621=CARTESIAN_POINT('Origin',(0.173205080756888,-0.4,0.));
#11622=CARTESIAN_POINT('',(0.0866025403784439,-0.4,0.15));
#11623=CARTESIAN_POINT('',(0.0866025403784439,-0.64,0.15));
#11624=CARTESIAN_POINT('Origin',(0.,-0.4,-2.77555756156289E-17));
#11625=CARTESIAN_POINT('Origin',(0.,-0.64,-2.77555756156289E-17));
#11863=UNCERTAINTY_MEASURE_WITH_UNIT(LENGTH_MEASURE(0.001),#11917,
'DISTANCE_ACCURACY_VALUE',
'Maximum model space distance between geometric entities at asserted c
onnectivities');
#11869=UNCERTAINTY_MEASURE_WITH_UNIT(LENGTH_MEASURE(0.001),#11917,
'DISTANCE_ACCURACY_VALUE',
'Maximum model space distance between geometric entities at asserted c
onnectivities');
#11910=(
GEOMETRIC_REPRESENTATION_CONTEXT(3)
GLOBAL_UNCERTAINTY_ASSIGNED_CONTEXT((#11863))
GLOBAL_UNIT_ASSIGNED_CONTEXT((#11917,#11919,#11920))
REPRESENTATION_CONTEXT('','3D')
);
#11916=(
GEOMETRIC_REPRESENTATION_CONTEXT(3)
GLOBAL_UNCERTAINTY_ASSIGNED_CONTEXT((#11869))
GLOBAL_UNIT_ASSIGNED_CONTEXT((#11917,#11919,#11920))
REPRESENTATION_CONTEXT('','3D')
);
#11917=(
LENGTH_UNIT()
NAMED_UNIT(*)
SI_UNIT(.CENTI.,.METRE.)
);
#11919=(
NAMED_UNIT(*)
PLANE_ANGLE_UNIT()
SI_UNIT($,.RADIAN.)
);
#11920=(
NAMED_UNIT(*)
SI_UNIT($,.STERADIAN.)
SOLID_ANGLE_UNIT()
);
#11961=SHAPE_DEFINITION_REPRESENTATION(#12012,#12119);
#12012=PRODUCT_DEFINITION_SHAPE('',$,#12166);
#12119=SHAPE_REPRESENTATION('',(#7264),#11910);
#12125=PRODUCT_DEFINITION_CONTEXT('part definition',#12265,'design');
#12166=PRODUCT_DEFINITION('Cap Screw - M4x16','Cap Screw - M4x16',#12212,
#12125);
#12212=PRODUCT_DEFINITION_FORMATION('',$,#12307);
#12265=APPLICATION_CONTEXT(
'Core Data for Automotive Mechanical Design Process');
#12266=PRODUCT_CONTEXT('part definition',#12265,'mechanical');
#12307=PRODUCT('Cap Screw - M4x16','Cap Screw - M4x16',
'Cap Screw - M4x16',(#12266));
#12376=COLOUR_RGB('Black',0.12,0.14,0.17);
#12377=FILL_AREA_STYLE_COLOUR('',#12376);
#12378=FILL_AREA_STYLE('',(#12377));
#12379=SURFACE_STYLE_FILL_AREA(#12378);
#12380=SURFACE_SIDE_STYLE('',(#12379));
#12381=SURFACE_STYLE_USAGE(.BOTH.,#12380);
#12382=PRESENTATION_STYLE_ASSIGNMENT((#12381));
ENDSEC;
END-ISO-10303-21;
